ISO-10303-21;
HEADER;
/* Generated by software containing ST-Developer
 * from STEP Tools, Inc. (www.steptools.com) 
 */

FILE_DESCRIPTION(
/* description */ ('Bell-crank linkage with push rods'),
/* implementation_level */ '2;1');

FILE_NAME(
/* name */ 'Cap Screw - M4x16.step',
/* time_stamp */ '2026-10-28T03:25:15-07:00',
/* author */ (''),
/* organization */ (''),
/* preprocessor_version */ 'ST-DEVELOPER v20.2',
/* originating_system */ 'Autodesk Translation Framework v15.17.0.0',
/* authorisation */ '');

FILE_SCHEMA (('AUTOMOTIVE_DESIGN { 1 0 10303 214 3 1 1 }'));
ENDSEC;

DATA;
#10=MECHANICAL_DESIGN_GEOMETRIC_PRESENTATION_REPRESENTATION('',(#641),#16678);
#443=CONICAL_SURFACE('',#10118,0.325,0.785398163397448);
#444=CONICAL_SURFACE('',#10122,0.335,0.785398163397448);
#445=CONICAL_SURFACE('',#10126,0.21,0.463647609000806);
#446=CONICAL_SURFACE('',#10130,0.18,0.785398163397448);
#452=ORIENTED_CLOSED_SHELL('',*,#8833,.F.);
#455=BREP_WITH_VOIDS('Body1',#8832,(#452));
#525=SHAPE_REPRESENTATION_RELATIONSHIP('SRR','None',#16943,#579);
#579=ADVANCED_BREP_SHAPE_REPRESENTATION('',(#455),#16648);
#641=STYLED_ITEM('',(#17298),#455);
#856=FACE_BOUND('',#2214,.T.);
#1123=PLANE('',#10116);
#1124=PLANE('',#10124);
#1125=PLANE('',#10132);
#1126=PLANE('',#10133);
#1127=PLANE('',#10134);
#1128=PLANE('',#10135);
#1129=PLANE('',#10136);
#1130=PLANE('',#10137);
#1131=PLANE('',#10138);
#1132=PLANE('',#10139);
#1133=PLANE('',#10140);
#1556=FACE_OUTER_BOUND('',#2209,.T.);
#1557=FACE_OUTER_BOUND('',#2210,.T.);
#1558=FACE_OUTER_BOUND('',#2211,.T.);
#1559=FACE_OUTER_BOUND('',#2212,.T.);
#1560=FACE_OUTER_BOUND('',#2213,.T.);
#1561=FACE_OUTER_BOUND('',#2215,.T.);
#1562=FACE_OUTER_BOUND('',#2216,.T.);
#1563=FACE_OUTER_BOUND('',#2217,.T.);
#1564=FACE_OUTER_BOUND('',#2218,.T.);
#1565=FACE_OUTER_BOUND('',#2219,.T.);
#1566=FACE_OUTER_BOUND('',#2220,.T.);
#1567=FACE_OUTER_BOUND('',#2221,.T.);
#1568=FACE_OUTER_BOUND('',#2222,.T.);
#1569=FACE_OUTER_BOUND('',#2223,.T.);
#1570=FACE_OUTER_BOUND('',#2224,.T.);
#1571=FACE_OUTER_BOUND('',#2225,.T.);
#1572=FACE_OUTER_BOUND('',#2226,.T.);
#2209=EDGE_LOOP('',(#7225));
#2210=EDGE_LOOP('',(#7226,#7227,#7228,#7229));
#2211=EDGE_LOOP('',(#7230,#7231,#7232,#7233));
#2212=EDGE_LOOP('',(#7234,#7235,#7236,#7237));
#2213=EDGE_LOOP('',(#7238));
#2214=EDGE_LOOP('',(#7239));
#2215=EDGE_LOOP('',(#7240,#7241,#7242,#7243));
#2216=EDGE_LOOP('',(#7244,#7245,#7246,#7247));
#2217=EDGE_LOOP('',(#7248,#7249,#7250,#7251));
#2218=EDGE_LOOP('',(#7252));
#2219=EDGE_LOOP('',(#7253,#7254,#7255,#7256));
#2220=EDGE_LOOP('',(#7257,#7258,#7259,#7260));
#2221=EDGE_LOOP('',(#7261,#7262,#7263,#7264));
#2222=EDGE_LOOP('',(#7265,#7266,#7267,#7268));
#2223=EDGE_LOOP('',(#7269,#7270,#7271,#7272));
#2224=EDGE_LOOP('',(#7273,#7274,#7275,#7276));
#2225=EDGE_LOOP('',(#7277,#7278,#7279,#7280,#7281,#7282));
#2226=EDGE_LOOP('',(#7283,#7284,#7285,#7286,#7287,#7288));
#2836=LINE('',#15520,#3385);
#2837=LINE('',#15524,#3386);
#2838=LINE('',#15528,#3387);
#2839=LINE('',#15535,#3388);
#2840=LINE('',#15539,#3389);
#2841=LINE('',#15543,#3390);
#2842=LINE('',#15548,#3391);
#2843=LINE('',#15550,#3392);
#2844=LINE('',#15552,#3393);
#2845=LINE('',#15553,#3394);
#2846=LINE('',#15556,#3395);
#2847=LINE('',#15558,#3396);
#2848=LINE('',#15559,#3397);
#2849=LINE('',#15562,#3398);
#2850=LINE('',#15564,#3399);
#2851=LINE('',#15565,#3400);
#2852=LINE('',#15568,#3401);
#2853=LINE('',#15570,#3402);
#2854=LINE('',#15571,#3403);
#2855=LINE('',#15574,#3404);
#2856=LINE('',#15576,#3405);
#2857=LINE('',#15577,#3406);
#2858=LINE('',#15579,#3407);
#2859=LINE('',#15580,#3408);
#3385=VECTOR('',#12266,0.325);
#3386=VECTOR('',#12271,0.35);
#3387=VECTOR('',#12276,0.335);
#3388=VECTOR('',#12285,0.21);
#3389=VECTOR('',#12290,0.2);
#3390=VECTOR('',#12295,0.18);
#3391=VECTOR('',#12300,1.);
#3392=VECTOR('',#12301,1.);
#3393=VECTOR('',#12302,1.);
#3394=VECTOR('',#12303,1.);
#3395=VECTOR('',#12306,1.);
#3396=VECTOR('',#12307,1.);
#3397=VECTOR('',#12308,1.);
#3398=VECTOR('',#12311,1.);
#3399=VECTOR('',#12312,1.);
#3400=VECTOR('',#12313,1.);
#3401=VECTOR('',#12316,1.);
#3402=VECTOR('',#12317,1.);
#3403=VECTOR('',#12318,1.);
#3404=VECTOR('',#12321,1.);
#3405=VECTOR('',#12322,1.);
#3406=VECTOR('',#12323,1.);
#3407=VECTOR('',#12326,1.);
#3408=VECTOR('',#12327,1.);
#3944=CIRCLE('',#10117,0.3);
#3945=CIRCLE('',#10119,0.35);
#3946=CIRCLE('',#10121,0.35);
#3947=CIRCLE('',#10123,0.32);
#3948=CIRCLE('',#10125,0.22);
#3949=CIRCLE('',#10127,0.1954);
#3950=CIRCLE('',#10129,0.1954);
#3951=CIRCLE('',#10131,0.16);
#4555=VERTEX_POINT('',#15515);
#4556=VERTEX_POINT('',#15518);
#4557=VERTEX_POINT('',#15522);
#4558=VERTEX_POINT('',#15526);
#4559=VERTEX_POINT('',#15530);
#4560=VERTEX_POINT('',#15533);
#4561=VERTEX_POINT('',#15537);
#4562=VERTEX_POINT('',#15541);
#4563=VERTEX_POINT('',#15546);
#4564=VERTEX_POINT('',#15547);
#4565=VERTEX_POINT('',#15549);
#4566=VERTEX_POINT('',#15551);
#4567=VERTEX_POINT('',#15555);
#4568=VERTEX_POINT('',#15557);
#4569=VERTEX_POINT('',#15561);
#4570=VERTEX_POINT('',#15563);
#4571=VERTEX_POINT('',#15567);
#4572=VERTEX_POINT('',#15569);
#4573=VERTEX_POINT('',#15573);
#4574=VERTEX_POINT('',#15575);
#5490=EDGE_CURVE('',#4555,#4555,#3944,.T.);
#5491=EDGE_CURVE('',#4556,#4556,#3945,.T.);
#5492=EDGE_CURVE('',#4556,#4555,#2836,.T.);
#5493=EDGE_CURVE('',#4557,#4557,#3946,.T.);
#5494=EDGE_CURVE('',#4557,#4556,#2837,.T.);
#5495=EDGE_CURVE('',#4558,#4558,#3947,.T.);
#5496=EDGE_CURVE('',#4558,#4557,#2838,.T.);
#5497=EDGE_CURVE('',#4559,#4559,#3948,.T.);
#5498=EDGE_CURVE('',#4560,#4560,#3949,.F.);
#5499=EDGE_CURVE('',#4560,#4559,#2839,.T.);
#5500=EDGE_CURVE('',#4561,#4561,#3950,.F.);
#5501=EDGE_CURVE('',#4561,#4560,#2840,.T.);
#5502=EDGE_CURVE('',#4562,#4562,#3951,.T.);
#5503=EDGE_CURVE('',#4562,#4561,#2841,.T.);
#5504=EDGE_CURVE('',#4563,#4564,#2842,.T.);
#5505=EDGE_CURVE('',#4564,#4565,#2843,.T.);
#5506=EDGE_CURVE('',#4565,#4566,#2844,.T.);
#5507=EDGE_CURVE('',#4563,#4566,#2845,.T.);
#5508=EDGE_CURVE('',#4564,#4567,#2846,.T.);
#5509=EDGE_CURVE('',#4567,#4568,#2847,.T.);
#5510=EDGE_CURVE('',#4568,#4565,#2848,.T.);
#5511=EDGE_CURVE('',#4567,#4569,#2849,.T.);
#5512=EDGE_CURVE('',#4569,#4570,#2850,.T.);
#5513=EDGE_CURVE('',#4570,#4568,#2851,.T.);
#5514=EDGE_CURVE('',#4569,#4571,#2852,.T.);
#5515=EDGE_CURVE('',#4571,#4572,#2853,.T.);
#5516=EDGE_CURVE('',#4572,#4570,#2854,.T.);
#5517=EDGE_CURVE('',#4571,#4573,#2855,.T.);
#5518=EDGE_CURVE('',#4573,#4574,#2856,.T.);
#5519=EDGE_CURVE('',#4574,#4572,#2857,.T.);
#5520=EDGE_CURVE('',#4573,#4563,#2858,.T.);
#5521=EDGE_CURVE('',#4566,#4574,#2859,.T.);
#7225=ORIENTED_EDGE('',*,*,#5490,.F.);
#7226=ORIENTED_EDGE('',*,*,#5491,.F.);
#7227=ORIENTED_EDGE('',*,*,#5492,.T.);
#7228=ORIENTED_EDGE('',*,*,#5490,.T.);
#7229=ORIENTED_EDGE('',*,*,#5492,.F.);
#7230=ORIENTED_EDGE('',*,*,#5493,.F.);
#7231=ORIENTED_EDGE('',*,*,#5494,.T.);
#7232=ORIENTED_EDGE('',*,*,#5491,.T.);
#7233=ORIENTED_EDGE('',*,*,#5494,.F.);
#7234=ORIENTED_EDGE('',*,*,#5495,.F.);
#7235=ORIENTED_EDGE('',*,*,#5496,.T.);
#7236=ORIENTED_EDGE('',*,*,#5493,.T.);
#7237=ORIENTED_EDGE('',*,*,#5496,.F.);
#7238=ORIENTED_EDGE('',*,*,#5495,.T.);
#7239=ORIENTED_EDGE('',*,*,#5497,.F.);
#7240=ORIENTED_EDGE('',*,*,#5498,.F.);
#7241=ORIENTED_EDGE('',*,*,#5499,.T.);
#7242=ORIENTED_EDGE('',*,*,#5497,.T.);
#7243=ORIENTED_EDGE('',*,*,#5499,.F.);
#7244=ORIENTED_EDGE('',*,*,#5500,.F.);
#7245=ORIENTED_EDGE('',*,*,#5501,.T.);
#7246=ORIENTED_EDGE('',*,*,#5498,.T.);
#7247=ORIENTED_EDGE('',*,*,#5501,.F.);
#7248=ORIENTED_EDGE('',*,*,#5502,.F.);
#7249=ORIENTED_EDGE('',*,*,#5503,.T.);
#7250=ORIENTED_EDGE('',*,*,#5500,.T.);
#7251=ORIENTED_EDGE('',*,*,#5503,.F.);
#7252=ORIENTED_EDGE('',*,*,#5502,.T.);
#7253=ORIENTED_EDGE('',*,*,#5504,.T.);
#7254=ORIENTED_EDGE('',*,*,#5505,.T.);
#7255=ORIENTED_EDGE('',*,*,#5506,.T.);
#7256=ORIENTED_EDGE('',*,*,#5507,.F.);
#7257=ORIENTED_EDGE('',*,*,#5508,.T.);
#7258=ORIENTED_EDGE('',*,*,#5509,.T.);
#7259=ORIENTED_EDGE('',*,*,#5510,.T.);
#7260=ORIENTED_EDGE('',*,*,#5505,.F.);
#7261=ORIENTED_EDGE('',*,*,#5511,.T.);
#7262=ORIENTED_EDGE('',*,*,#5512,.T.);
#7263=ORIENTED_EDGE('',*,*,#5513,.T.);
#7264=ORIENTED_EDGE('',*,*,#5509,.F.);
#7265=ORIENTED_EDGE('',*,*,#5514,.T.);
#7266=ORIENTED_EDGE('',*,*,#5515,.T.);
#7267=ORIENTED_EDGE('',*,*,#5516,.T.);
#7268=ORIENTED_EDGE('',*,*,#5512,.F.);
#7269=ORIENTED_EDGE('',*,*,#5517,.T.);
#7270=ORIENTED_EDGE('',*,*,#5518,.T.);
#7271=ORIENTED_EDGE('',*,*,#5519,.T.);
#7272=ORIENTED_EDGE('',*,*,#5515,.F.);
#7273=ORIENTED_EDGE('',*,*,#5520,.T.);
#7274=ORIENTED_EDGE('',*,*,#5507,.T.);
#7275=ORIENTED_EDGE('',*,*,#5521,.T.);
#7276=ORIENTED_EDGE('',*,*,#5518,.F.);
#7277=ORIENTED_EDGE('',*,*,#5520,.F.);
#7278=ORIENTED_EDGE('',*,*,#5517,.F.);
#7279=ORIENTED_EDGE('',*,*,#5514,.F.);
#7280=ORIENTED_EDGE('',*,*,#5511,.F.);
#7281=ORIENTED_EDGE('',*,*,#5508,.F.);
#7282=ORIENTED_EDGE('',*,*,#5504,.F.);
#7283=ORIENTED_EDGE('',*,*,#5521,.F.);
#7284=ORIENTED_EDGE('',*,*,#5506,.F.);
#7285=ORIENTED_EDGE('',*,*,#5510,.F.);
#7286=ORIENTED_EDGE('',*,*,#5513,.F.);
#7287=ORIENTED_EDGE('',*,*,#5516,.F.);
#7288=ORIENTED_EDGE('',*,*,#5519,.F.);
#8191=CYLINDRICAL_SURFACE('',#10120,0.35);
#8192=CYLINDRICAL_SURFACE('',#10128,0.1954);
#8581=ADVANCED_FACE('',(#1556),#1123,.T.);
#8582=ADVANCED_FACE('',(#1557),#443,.T.);
#8583=ADVANCED_FACE('',(#1558),#8191,.T.);
#8584=ADVANCED_FACE('',(#1559),#444,.T.);
#8585=ADVANCED_FACE('',(#1560,#856),#1124,.T.);
#8586=ADVANCED_FACE('',(#1561),#445,.T.);
#8587=ADVANCED_FACE('',(#1562),#8192,.T.);
#8588=ADVANCED_FACE('',(#1563),#446,.T.);
#8589=ADVANCED_FACE('',(#1564),#1125,.T.);
#8590=ADVANCED_FACE('',(#1565),#1126,.F.);
#8591=ADVANCED_FACE('',(#1566),#1127,.F.);
#8592=ADVANCED_FACE('',(#1567),#1128,.F.);
#8593=ADVANCED_FACE('',(#1568),#1129,.F.);
#8594=ADVANCED_FACE('',(#1569),#1130,.F.);
#8595=ADVANCED_FACE('',(#1570),#1131,.F.);
#8596=ADVANCED_FACE('',(#1571),#1132,.F.);
#8597=ADVANCED_FACE('',(#1572),#1133,.F.);
#8832=CLOSED_SHELL('',(#8581,#8582,#8583,#8584,#8585,#8586,#8587,#8588,
#8589));
#8833=CLOSED_SHELL('',(#8590,#8591,#8592,#8593,#8594,#8595,#8596,#8597));
#10115=AXIS2_PLACEMENT_3D('',#15513,#12256,#12257);
#10116=AXIS2_PLACEMENT_3D('',#15514,#12258,#12259);
#10117=AXIS2_PLACEMENT_3D('',#15516,#12260,#12261);
#10118=AXIS2_PLACEMENT_3D('',#15517,#12262,#12263);
#10119=AXIS2_PLACEMENT_3D('',#15519,#12264,#12265);
#10120=AXIS2_PLACEMENT_3D('',#15521,#12267,#12268);
#10121=AXIS2_PLACEMENT_3D('',#15523,#12269,#12270);
#10122=AXIS2_PLACEMENT_3D('',#15525,#12272,#12273);
#10123=AXIS2_PLACEMENT_3D('',#15527,#12274,#12275);
#10124=AXIS2_PLACEMENT_3D('',#15529,#12277,#12278);
#10125=AXIS2_PLACEMENT_3D('',#15531,#12279,#12280);
#10126=AXIS2_PLACEMENT_3D('',#15532,#12281,#12282);
#10127=AXIS2_PLACEMENT_3D('',#15534,#12283,#12284);
#10128=AXIS2_PLACEMENT_3D('',#15536,#12286,#12287);
#10129=AXIS2_PLACEMENT_3D('',#15538,#12288,#12289);
#10130=AXIS2_PLACEMENT_3D('',#15540,#12291,#12292);
#10131=AXIS2_PLACEMENT_3D('',#15542,#12293,#12294);
#10132=AXIS2_PLACEMENT_3D('',#15544,#12296,#12297);
#10133=AXIS2_PLACEMENT_3D('',#15545,#12298,#12299);
#10134=AXIS2_PLACEMENT_3D('',#15554,#12304,#12305);
#10135=AXIS2_PLACEMENT_3D('',#15560,#12309,#12310);
#10136=AXIS2_PLACEMENT_3D('',#15566,#12314,#12315);
#10137=AXIS2_PLACEMENT_3D('',#15572,#12319,#12320);
#10138=AXIS2_PLACEMENT_3D('',#15578,#12324,#12325);
#10139=AXIS2_PLACEMENT_3D('',#15581,#12328,#12329);
#10140=AXIS2_PLACEMENT_3D('',#15582,#12330,#12331);
#12256=DIRECTION('axis',(0.,0.,1.));
#12257=DIRECTION('refdir',(1.,0.,0.));
#12258=DIRECTION('center_axis',(0.,1.,0.));
#12259=DIRECTION('ref_axis',(0.,0.,1.));
#12260=DIRECTION('center_axis',(0.,-1.,0.));
#12261=DIRECTION('ref_axis',(1.,0.,0.));
#12262=DIRECTION('center_axis',(0.,-1.,0.));
#12263=DIRECTION('ref_axis',(1.,0.,0.));
#12264=DIRECTION('center_axis',(0.,-1.,0.));
#12265=DIRECTION('ref_axis',(1.,0.,0.));
#12266=DIRECTION('',(0.707106781186547,0.707106781186548,8.65956056235493E-17));
#12267=DIRECTION('center_axis',(0.,-1.,0.));
#12268=DIRECTION('ref_axis',(1.,0.,0.));
#12269=DIRECTION('center_axis',(0.,-1.,0.));
#12270=DIRECTION('ref_axis',(1.,0.,0.));
#12271=DIRECTION('',(0.,1.,0.));
#12272=DIRECTION('center_axis',(0.,1.,0.));
#12273=DIRECTION('ref_axis',(1.,0.,0.));
#12274=DIRECTION('center_axis',(0.,-1.,0.));
#12275=DIRECTION('ref_axis',(1.,0.,0.));
#12276=DIRECTION('',(-0.707106781186547,0.707106781186548,-8.65956056235493E-17));
#12277=DIRECTION('center_axis',(0.,-1.,0.));
#12278=DIRECTION('ref_axis',(0.,0.,-1.));
#12279=DIRECTION('center_axis',(0.,-1.,0.));
#12280=DIRECTION('ref_axis',(1.,0.,0.));
#12281=DIRECTION('center_axis',(0.,1.,0.));
#12282=DIRECTION('ref_axis',(1.,0.,0.));
#12283=DIRECTION('center_axis',(0.,1.,0.));
#12284=DIRECTION('ref_axis',(1.,0.,0.));
#12285=DIRECTION('',(-0.447213595499958,0.894427190999916,-5.47678698264203E-17));
#12286=DIRECTION('center_axis',(0.,-1.,0.));
#12287=DIRECTION('ref_axis',(1.,0.,0.));
#12288=DIRECTION('center_axis',(0.,1.,0.));
#12289=DIRECTION('ref_axis',(1.,0.,0.));
#12290=DIRECTION('',(0.,1.,0.));
#12291=DIRECTION('center_axis',(0.,1.,0.));
#12292=DIRECTION('ref_axis',(1.,0.,0.));
#12293=DIRECTION('center_axis',(0.,-1.,0.));
#12294=DIRECTION('ref_axis',(1.,0.,0.));
#12295=DIRECTION('',(-0.707106781186547,0.707106781186548,-8.65956056235493E-17));
#12296=DIRECTION('center_axis',(0.,-1.,0.));
#12297=DIRECTION('ref_axis',(0.,0.,-1.));
#12298=DIRECTION('center_axis',(0.866025403784439,0.,-0.5));
#12299=DIRECTION('ref_axis',(0.5,0.,0.866025403784439));
#12300=DIRECTION('',(-0.5,0.,-0.866025403784439));
#12301=DIRECTION('',(0.,-1.,0.));
#12302=DIRECTION('',(0.5,0.,0.866025403784439));
#12303=DIRECTION('',(0.,-1.,0.));
#12304=DIRECTION('center_axis',(1.60246890531964E-16,0.,-1.));
#12305=DIRECTION('ref_axis',(1.,0.,1.60246890531964E-16));
#12306=DIRECTION('',(-1.,0.,-1.60246890531964E-16));
#12307=DIRECTION('',(0.,-1.,0.));
#12308=DIRECTION('',(1.,0.,1.60246890531964E-16));
#12309=DIRECTION('center_axis',(-0.866025403784439,0.,-0.5));
#12310=DIRECTION('ref_axis',(0.5,0.,-0.866025403784439));
#12311=DIRECTION('',(-0.5,0.,0.866025403784439));
#12312=DIRECTION('',(0.,-1.,0.));
#12313=DIRECTION('',(0.5,0.,-0.866025403784439));
#12314=DIRECTION('center_axis',(-0.866025403784439,0.,0.5));
#12315=DIRECTION('ref_axis',(-0.5,0.,-0.866025403784439));
#12316=DIRECTION('',(0.5,0.,0.866025403784439));
#12317=DIRECTION('',(0.,-1.,0.));
#12318=DIRECTION('',(-0.5,0.,-0.866025403784439));
#12319=DIRECTION('center_axis',(-1.60246890531964E-16,0.,1.));
#12320=DIRECTION('ref_axis',(-1.,0.,-1.60246890531964E-16));
#12321=DIRECTION('',(1.,0.,1.60246890531964E-16));
#12322=DIRECTION('',(0.,-1.,0.));
#12323=DIRECTION('',(-1.,0.,-1.60246890531964E-16));
#12324=DIRECTION('center_axis',(0.866025403784439,0.,0.5));
#12325=DIRECTION('ref_axis',(-0.5,0.,0.866025403784439));
#12326=DIRECTION('',(0.5,0.,-0.866025403784439));
#12327=DIRECTION('',(-0.5,0.,0.866025403784439));
#12328=DIRECTION('center_axis',(0.,1.,0.));
#12329=DIRECTION('ref_axis',(1.,0.,0.));
#12330=DIRECTION('center_axis',(0.,-1.,0.));
#12331=DIRECTION('ref_axis',(0.,0.,-1.));
#15513=CARTESIAN_POINT('',(0.,0.,0.));
#15514=CARTESIAN_POINT('Origin',(0.3,0.4,0.));
#15515=CARTESIAN_POINT('',(-0.3,0.4,-3.67394039744206E-17));
#15516=CARTESIAN_POINT('Origin',(0.,0.4,0.));
#15517=CARTESIAN_POINT('Origin',(0.,0.375,0.));
#15518=CARTESIAN_POINT('',(-0.35,0.35,-4.28626379701573E-17));
#15519=CARTESIAN_POINT('Origin',(0.,0.35,0.));
#15520=CARTESIAN_POINT('',(-0.325,0.375,-3.9801020972289E-17));
#15521=CARTESIAN_POINT('Origin',(0.,0.19,0.));
#15522=CARTESIAN_POINT('',(-0.35,0.03,-4.28626379701574E-17));
#15523=CARTESIAN_POINT('Origin',(0.,0.03,0.));
#15524=CARTESIAN_POINT('',(-0.35,0.19,-4.28626379701574E-17));
#15525=CARTESIAN_POINT('Origin',(0.,0.0149999999999999,0.));
#15526=CARTESIAN_POINT('',(-0.32,-3.29597460435593E-17,-3.91886975727153E-17));
#15527=CARTESIAN_POINT('Origin',(0.,0.,0.));
#15528=CARTESIAN_POINT('',(-0.335,0.0149999999999999,-4.10256677714363E-17));
#15529=CARTESIAN_POINT('Origin',(0.22,0.,0.));
#15530=CARTESIAN_POINT('',(-0.22,-6.93889390390723E-18,-2.69422295812418E-17));
#15531=CARTESIAN_POINT('Origin',(0.,0.,0.));
#15532=CARTESIAN_POINT('Origin',(0.,-0.02,0.));
#15533=CARTESIAN_POINT('',(-0.1954,-0.0492,2.39295984553393E-17));
#15534=CARTESIAN_POINT('Origin',(0.,-0.0492,0.));
#15535=CARTESIAN_POINT('',(-0.21,-0.02,-2.57175827820944E-17));
#15536=CARTESIAN_POINT('Origin',(0.,-0.8,0.));
#15537=CARTESIAN_POINT('',(-0.1954,-1.5646,2.39295984553393E-17));
#15538=CARTESIAN_POINT('Origin',(0.,-1.5646,0.));
#15539=CARTESIAN_POINT('',(-0.1954,-0.8,-2.39295984553393E-17));
#15540=CARTESIAN_POINT('Origin',(0.,-1.58,0.));
#15541=CARTESIAN_POINT('',(-0.16,-1.6,-1.95943487863577E-17));
#15542=CARTESIAN_POINT('Origin',(0.,-1.6,0.));
#15543=CARTESIAN_POINT('',(-0.18,-1.58,-2.20436423846524E-17));
#15544=CARTESIAN_POINT('Origin',(0.,-1.6,0.));
#15545=CARTESIAN_POINT('Origin',(0.0866025403784439,-0.4,-0.15));
#15546=CARTESIAN_POINT('',(0.173205080756888,-0.4,0.));
#15547=CARTESIAN_POINT('',(0.0866025403784439,-0.4,-0.15));
#15548=CARTESIAN_POINT('',(0.173205080756888,-0.4,0.));
#15549=CARTESIAN_POINT('',(0.0866025403784439,-0.64,-0.15));
#15550=CARTESIAN_POINT('',(0.0866025403784439,-0.4,-0.15));
#15551=CARTESIAN_POINT('',(0.173205080756888,-0.64,0.));
#15552=CARTESIAN_POINT('',(0.173205080756888,-0.64,0.));
#15553=CARTESIAN_POINT('',(0.173205080756888,-0.4,0.));
#15554=CARTESIAN_POINT('Origin',(-0.0866025403784438,-0.4,-0.15));
#15555=CARTESIAN_POINT('',(-0.0866025403784438,-0.4,-0.15));
#15556=CARTESIAN_POINT('',(0.0866025403784439,-0.4,-0.15));
#15557=CARTESIAN_POINT('',(-0.0866025403784438,-0.64,-0.15));
#15558=CARTESIAN_POINT('',(-0.0866025403784438,-0.4,-0.15));
#15559=CARTESIAN_POINT('',(0.0866025403784439,-0.64,-0.15));
#15560=CARTESIAN_POINT('Origin',(-0.173205080756888,-0.4,-2.77555756156289E-17));
#15561=CARTESIAN_POINT('',(-0.173205080756888,-0.4,-2.12115047744981E-17));
#15562=CARTESIAN_POINT('',(-0.0866025403784438,-0.4,-0.15));
#15563=CARTESIAN_POINT('',(-0.173205080756888,-0.64,-2.77555756156289E-17));
#15564=CARTESIAN_POINT('',(-0.173205080756888,-0.4,-2.12115047744981E-17));
#15565=CARTESIAN_POINT('',(-0.0866025403784438,-0.64,-0.15));
#15566=CARTESIAN_POINT('Origin',(-0.0866025403784439,-0.4,0.15));
#15567=CARTESIAN_POINT('',(-0.0866025403784439,-0.4,0.15));
#15568=CARTESIAN_POINT('',(-0.173205080756888,-0.4,-2.12115047744981E-17));
#15569=CARTESIAN_POINT('',(-0.0866025403784439,-0.64,0.15));
#15570=CARTESIAN_POINT('',(-0.0866025403784439,-0.4,0.15));
#15571=CARTESIAN_POINT('',(-0.173205080756888,-0.64,-2.12115047744981E-17));
#15572=CARTESIAN_POINT('Origin',(0.0866025403784439,-0.4,0.15));
#15573=CARTESIAN_POINT('',(0.0866025403784439,-0.4,0.15));
#15574=CARTESIAN_POINT('',(-0.0866025403784439,-0.4,0.15));
#15575=CARTESIAN_POINT('',(0.0866025403784439,-0.64,0.15));
#15576=CARTESIAN_POINT('',(0.0866025403784439,-0.4,0.15));
#15577=CARTESIAN_POINT('',(-0.0866025403784439,-0.64,0.15));
#15578=CARTESIAN_POINT('Origin',(0.173205080756888,-0.4,0.));
#15579=CARTESIAN_POINT('',(0.0866025403784439,-0.4,0.15));
#15580=CARTESIAN_POINT('',(0.0866025403784439,-0.64,0.15));
#15581=CARTESIAN_POINT('Origin',(0.,-0.4,-2.77555756156289E-17));
#15582=CARTESIAN_POINT('Origin',(0.,-0.64,-2.77555756156289E-17));
#16584=UNCERTAINTY_MEASURE_WITH_UNIT(LENGTH_MEASURE(0.001),#16679,
'DISTANCE_ACCURACY_VALUE',
'Maximum model space distance between geometric entities at asserted c
onnectivities');
#16614=UNCERTAINTY_MEASURE_WITH_UNIT(LENGTH_MEASURE(0.001),#16679,
'DISTANCE_ACCURACY_VALUE',
'Maximum model space distance between geometric entities at asserted c
onnectivities');
#16648=(
GEOMETRIC_REPRESENTATION_CONTEXT(3)
GLOBAL_UNCERTAINTY_ASSIGNED_CONTEXT((#16584))
GLOBAL_UNIT_ASSIGNED_CONTEXT((#16679,#16681,#16682))
REPRESENTATION_CONTEXT('','3D')
);
#16678=(
GEOMETRIC_REPRESENTATION_CONTEXT(3)
GLOBAL_UNCERTAINTY_ASSIGNED_CONTEXT((#16614))
GLOBAL_UNIT_ASSIGNED_CONTEXT((#16679,#16681,#16682))
REPRESENTATION_CONTEXT('','3D')
);
#16679=(
LENGTH_UNIT()
NAMED_UNIT(*)
SI_UNIT(.CENTI.,.METRE.)
);
#16681=(
NAMED_UNIT(*)
PLANE_ANGLE_UNIT()
SI_UNIT($,.RADIAN.)
);
#16682=(
NAMED_UNIT(*)
SI_UNIT($,.STERADIAN.)
SOLID_ANGLE_UNIT()
);
#16716=SHAPE_DEFINITION_REPRESENTATION(#16784,#16943);
#16784=PRODUCT_DEFINITION_SHAPE('',$,#17007);
#16943=SHAPE_REPRESENTATION('',(#10115),#16648);
#16973=PRODUCT_DEFINITION_CONTEXT('part definition',#17164,'design');
#17007=PRODUCT_DEFINITION('Cap Screw - M4x16','Cap Screw - M4x16',#17070,
#16973);
#17070=PRODUCT_DEFINITION_FORMATION('',$,#17199);
#17164=APPLICATION_CONTEXT(
'Core Data for Automotive Mechanical Design Process');
#17165=PRODUCT_CONTEXT('part definition',#17164,'mechanical');
#17199=PRODUCT('Cap Screw - M4x16','Cap Screw - M4x16',
'Cap Screw - M4x16',(#17165));
#17292=COLOUR_RGB('Black',0.12,0.14,0.17);
#17293=FILL_AREA_STYLE_COLOUR('',#17292);
#17294=FILL_AREA_STYLE('',(#17293));
#17295=SURFACE_STYLE_FILL_AREA(#17294);
#17296=SURFACE_SIDE_STYLE('',(#17295));
#17297=SURFACE_STYLE_USAGE(.BOTH.,#17296);
#17298=PRESENTATION_STYLE_ASSIGNMENT((#17297));
ENDSEC;
END-ISO-10303-21;
